ISO-10303-21;
HEADER;
/* Generated by software containing ST-Developer
 * from STEP Tools, Inc. (www.steptools.com) 
 */

FILE_DESCRIPTION(
/* description */ ('Five-roller gravity conveyor'),
/* implementation_level */ '2;1');

FILE_NAME(
/* name */ 'M5x14 Cap Screw.step',
/* time_stamp */ '2026-10-29T15:36:43-07:00',
/* author */ (''),
/* organization */ (''),
/* preprocessor_version */ 'ST-DEVELOPER v20.2',
/* originating_system */ 'Autodesk Translation Framework v15.17.0.0',
/* authorisation */ '');

FILE_SCHEMA (('AUTOMOTIVE_DESIGN { 1 0 10303 214 3 1 1 }'));
ENDSEC;

DATA;
#10=MECHANICAL_DESIGN_GEOMETRIC_PRESENTATION_REPRESENTATION('',(#316),#7806);
#261=CONICAL_SURFACE('',#4586,0.4,0.785398163397448);
#262=CONICAL_SURFACE('',#4590,0.41,0.785398163397448);
#263=CONICAL_SURFACE('',#4594,0.26,0.463647609000806);
#272=ORIENTED_CLOSED_SHELL('',*,#4203,.F.);
#274=BREP_WITH_VOIDS('Body1',#4204,(#272));
#280=SHAPE_REPRESENTATION_RELATIONSHIP('SRR','None',#7917,#298);
#298=ADVANCED_BREP_SHAPE_REPRESENTATION('',(#274),#7790);
#316=STYLED_ITEM('',(#8098),#274);
#380=FACE_BOUND('',#1016,.T.);
#461=CIRCLE('',#4583,0.24505);
#462=CIRCLE('',#4585,0.375);
#463=CIRCLE('',#4587,0.425);
#464=CIRCLE('',#4589,0.425);
#465=CIRCLE('',#4591,0.395);
#466=CIRCLE('',#4593,0.27);
#467=CIRCLE('',#4595,0.24505);
#614=CYLINDRICAL_SURFACE('',#4588,0.425);
#615=CYLINDRICAL_SURFACE('',#4596,0.24505);
#752=FACE_OUTER_BOUND('',#1002,.T.);
#753=FACE_OUTER_BOUND('',#1003,.T.);
#754=FACE_OUTER_BOUND('',#1004,.T.);
#755=FACE_OUTER_BOUND('',#1005,.T.);
#756=FACE_OUTER_BOUND('',#1006,.T.);
#757=FACE_OUTER_BOUND('',#1007,.T.);
#758=FACE_OUTER_BOUND('',#1008,.T.);
#759=FACE_OUTER_BOUND('',#1009,.T.);
#760=FACE_OUTER_BOUND('',#1010,.T.);
#761=FACE_OUTER_BOUND('',#1011,.T.);
#762=FACE_OUTER_BOUND('',#1012,.T.);
#763=FACE_OUTER_BOUND('',#1013,.T.);
#764=FACE_OUTER_BOUND('',#1014,.T.);
#765=FACE_OUTER_BOUND('',#1015,.T.);
#766=FACE_OUTER_BOUND('',#1017,.T.);
#767=FACE_OUTER_BOUND('',#1018,.T.);
#1002=EDGE_LOOP('',(#3282,#3283,#3284,#3285));
#1003=EDGE_LOOP('',(#3286,#3287,#3288,#3289));
#1004=EDGE_LOOP('',(#3290,#3291,#3292,#3293));
#1005=EDGE_LOOP('',(#3294,#3295,#3296,#3297));
#1006=EDGE_LOOP('',(#3298,#3299,#3300,#3301));
#1007=EDGE_LOOP('',(#3302,#3303,#3304,#3305));
#1008=EDGE_LOOP('',(#3306,#3307,#3308,#3309,#3310,#3311));
#1009=EDGE_LOOP('',(#3312,#3313,#3314,#3315,#3316,#3317));
#1010=EDGE_LOOP('',(#3318));
#1011=EDGE_LOOP('',(#3319));
#1012=EDGE_LOOP('',(#3320,#3321,#3322,#3323));
#1013=EDGE_LOOP('',(#3324,#3325,#3326,#3327));
#1014=EDGE_LOOP('',(#3328,#3329,#3330,#3331));
#1015=EDGE_LOOP('',(#3332));
#1016=EDGE_LOOP('',(#3333));
#1017=EDGE_LOOP('',(#3334,#3335,#3336,#3337));
#1018=EDGE_LOOP('',(#3338,#3339,#3340,#3341));
#1399=LINE('',#6767,#1740);
#1400=LINE('',#6769,#1741);
#1401=LINE('',#6771,#1742);
#1402=LINE('',#6772,#1743);
#1403=LINE('',#6775,#1744);
#1404=LINE('',#6777,#1745);
#1405=LINE('',#6778,#1746);
#1406=LINE('',#6781,#1747);
#1407=LINE('',#6783,#1748);
#1408=LINE('',#6784,#1749);
#1409=LINE('',#6787,#1750);
#1410=LINE('',#6789,#1751);
#1411=LINE('',#6790,#1752);
#1412=LINE('',#6793,#1753);
#1413=LINE('',#6795,#1754);
#1414=LINE('',#6796,#1755);
#1415=LINE('',#6798,#1756);
#1416=LINE('',#6799,#1757);
#1417=LINE('',#6811,#1758);
#1418=LINE('',#6815,#1759);
#1419=LINE('',#6819,#1760);
#1420=LINE('',#6826,#1761);
#1421=LINE('',#6828,#1762);
#1740=VECTOR('',#5431,1.);
#1741=VECTOR('',#5432,1.);
#1742=VECTOR('',#5433,1.);
#1743=VECTOR('',#5434,1.);
#1744=VECTOR('',#5437,1.);
#1745=VECTOR('',#5438,1.);
#1746=VECTOR('',#5439,1.);
#1747=VECTOR('',#5442,1.);
#1748=VECTOR('',#5443,1.);
#1749=VECTOR('',#5444,1.);
#1750=VECTOR('',#5447,1.);
#1751=VECTOR('',#5448,1.);
#1752=VECTOR('',#5449,1.);
#1753=VECTOR('',#5452,1.);
#1754=VECTOR('',#5453,1.);
#1755=VECTOR('',#5454,1.);
#1756=VECTOR('',#5457,1.);
#1757=VECTOR('',#5458,1.);
#1758=VECTOR('',#5475,0.4);
#1759=VECTOR('',#5480,0.425);
#1760=VECTOR('',#5485,0.41);
#1761=VECTOR('',#5494,0.26);
#1762=VECTOR('',#5497,0.25);
#2033=VERTEX_POINT('',#6765);
#2034=VERTEX_POINT('',#6766);
#2035=VERTEX_POINT('',#6768);
#2036=VERTEX_POINT('',#6770);
#2037=VERTEX_POINT('',#6774);
#2038=VERTEX_POINT('',#6776);
#2039=VERTEX_POINT('',#6780);
#2040=VERTEX_POINT('',#6782);
#2041=VERTEX_POINT('',#6786);
#2042=VERTEX_POINT('',#6788);
#2043=VERTEX_POINT('',#6792);
#2044=VERTEX_POINT('',#6794);
#2045=VERTEX_POINT('',#6803);
#2046=VERTEX_POINT('',#6806);
#2047=VERTEX_POINT('',#6809);
#2048=VERTEX_POINT('',#6813);
#2049=VERTEX_POINT('',#6817);
#2050=VERTEX_POINT('',#6821);
#2051=VERTEX_POINT('',#6824);
#2484=EDGE_CURVE('',#2033,#2034,#1399,.T.);
#2485=EDGE_CURVE('',#2034,#2035,#1400,.T.);
#2486=EDGE_CURVE('',#2035,#2036,#1401,.T.);
#2487=EDGE_CURVE('',#2033,#2036,#1402,.T.);
#2488=EDGE_CURVE('',#2034,#2037,#1403,.T.);
#2489=EDGE_CURVE('',#2037,#2038,#1404,.T.);
#2490=EDGE_CURVE('',#2038,#2035,#1405,.T.);
#2491=EDGE_CURVE('',#2037,#2039,#1406,.T.);
#2492=EDGE_CURVE('',#2039,#2040,#1407,.T.);
#2493=EDGE_CURVE('',#2040,#2038,#1408,.T.);
#2494=EDGE_CURVE('',#2039,#2041,#1409,.T.);
#2495=EDGE_CURVE('',#2041,#2042,#1410,.T.);
#2496=EDGE_CURVE('',#2042,#2040,#1411,.T.);
#2497=EDGE_CURVE('',#2041,#2043,#1412,.T.);
#2498=EDGE_CURVE('',#2043,#2044,#1413,.T.);
#2499=EDGE_CURVE('',#2044,#2042,#1414,.T.);
#2500=EDGE_CURVE('',#2043,#2033,#1415,.T.);
#2501=EDGE_CURVE('',#2036,#2044,#1416,.T.);
#2502=EDGE_CURVE('',#2045,#2045,#461,.T.);
#2503=EDGE_CURVE('',#2046,#2046,#462,.T.);
#2504=EDGE_CURVE('',#2047,#2047,#463,.T.);
#2505=EDGE_CURVE('',#2047,#2046,#1417,.T.);
#2506=EDGE_CURVE('',#2048,#2048,#464,.T.);
#2507=EDGE_CURVE('',#2048,#2047,#1418,.T.);
#2508=EDGE_CURVE('',#2049,#2049,#465,.T.);
#2509=EDGE_CURVE('',#2049,#2048,#1419,.T.);
#2510=EDGE_CURVE('',#2050,#2050,#466,.T.);
#2511=EDGE_CURVE('',#2051,#2051,#467,.F.);
#2512=EDGE_CURVE('',#2051,#2050,#1420,.T.);
#2513=EDGE_CURVE('',#2045,#2051,#1421,.T.);
#3282=ORIENTED_EDGE('',*,*,#2484,.T.);
#3283=ORIENTED_EDGE('',*,*,#2485,.T.);
#3284=ORIENTED_EDGE('',*,*,#2486,.T.);
#3285=ORIENTED_EDGE('',*,*,#2487,.F.);
#3286=ORIENTED_EDGE('',*,*,#2488,.T.);
#3287=ORIENTED_EDGE('',*,*,#2489,.T.);
#3288=ORIENTED_EDGE('',*,*,#2490,.T.);
#3289=ORIENTED_EDGE('',*,*,#2485,.F.);
#3290=ORIENTED_EDGE('',*,*,#2491,.T.);
#3291=ORIENTED_EDGE('',*,*,#2492,.T.);
#3292=ORIENTED_EDGE('',*,*,#2493,.T.);
#3293=ORIENTED_EDGE('',*,*,#2489,.F.);
#3294=ORIENTED_EDGE('',*,*,#2494,.T.);
#3295=ORIENTED_EDGE('',*,*,#2495,.T.);
#3296=ORIENTED_EDGE('',*,*,#2496,.T.);
#3297=ORIENTED_EDGE('',*,*,#2492,.F.);
#3298=ORIENTED_EDGE('',*,*,#2497,.T.);
#3299=ORIENTED_EDGE('',*,*,#2498,.T.);
#3300=ORIENTED_EDGE('',*,*,#2499,.T.);
#3301=ORIENTED_EDGE('',*,*,#2495,.F.);
#3302=ORIENTED_EDGE('',*,*,#2500,.T.);
#3303=ORIENTED_EDGE('',*,*,#2487,.T.);
#3304=ORIENTED_EDGE('',*,*,#2501,.T.);
#3305=ORIENTED_EDGE('',*,*,#2498,.F.);
#3306=ORIENTED_EDGE('',*,*,#2500,.F.);
#3307=ORIENTED_EDGE('',*,*,#2497,.F.);
#3308=ORIENTED_EDGE('',*,*,#2494,.F.);
#3309=ORIENTED_EDGE('',*,*,#2491,.F.);
#3310=ORIENTED_EDGE('',*,*,#2488,.F.);
#3311=ORIENTED_EDGE('',*,*,#2484,.F.);
#3312=ORIENTED_EDGE('',*,*,#2501,.F.);
#3313=ORIENTED_EDGE('',*,*,#2486,.F.);
#3314=ORIENTED_EDGE('',*,*,#2490,.F.);
#3315=ORIENTED_EDGE('',*,*,#2493,.F.);
#3316=ORIENTED_EDGE('',*,*,#2496,.F.);
#3317=ORIENTED_EDGE('',*,*,#2499,.F.);
#3318=ORIENTED_EDGE('',*,*,#2502,.F.);
#3319=ORIENTED_EDGE('',*,*,#2503,.F.);
#3320=ORIENTED_EDGE('',*,*,#2504,.F.);
#3321=ORIENTED_EDGE('',*,*,#2505,.T.);
#3322=ORIENTED_EDGE('',*,*,#2503,.T.);
#3323=ORIENTED_EDGE('',*,*,#2505,.F.);
#3324=ORIENTED_EDGE('',*,*,#2506,.F.);
#3325=ORIENTED_EDGE('',*,*,#2507,.T.);
#3326=ORIENTED_EDGE('',*,*,#2504,.T.);
#3327=ORIENTED_EDGE('',*,*,#2507,.F.);
#3328=ORIENTED_EDGE('',*,*,#2508,.F.);
#3329=ORIENTED_EDGE('',*,*,#2509,.T.);
#3330=ORIENTED_EDGE('',*,*,#2506,.T.);
#3331=ORIENTED_EDGE('',*,*,#2509,.F.);
#3332=ORIENTED_EDGE('',*,*,#2508,.T.);
#3333=ORIENTED_EDGE('',*,*,#2510,.F.);
#3334=ORIENTED_EDGE('',*,*,#2511,.F.);
#3335=ORIENTED_EDGE('',*,*,#2512,.T.);
#3336=ORIENTED_EDGE('',*,*,#2510,.T.);
#3337=ORIENTED_EDGE('',*,*,#2512,.F.);
#3338=ORIENTED_EDGE('',*,*,#2502,.T.);
#3339=ORIENTED_EDGE('',*,*,#2513,.T.);
#3340=ORIENTED_EDGE('',*,*,#2511,.T.);
#3341=ORIENTED_EDGE('',*,*,#2513,.F.);
#3902=PLANE('',#4574);
#3903=PLANE('',#4575);
#3904=PLANE('',#4576);
#3905=PLANE('',#4577);
#3906=PLANE('',#4578);
#3907=PLANE('',#4579);
#3908=PLANE('',#4580);
#3909=PLANE('',#4581);
#3910=PLANE('',#4582);
#3911=PLANE('',#4584);
#3912=PLANE('',#4592);
#4067=ADVANCED_FACE('',(#752),#3902,.F.);
#4068=ADVANCED_FACE('',(#753),#3903,.F.);
#4069=ADVANCED_FACE('',(#754),#3904,.F.);
#4070=ADVANCED_FACE('',(#755),#3905,.F.);
#4071=ADVANCED_FACE('',(#756),#3906,.F.);
#4072=ADVANCED_FACE('',(#757),#3907,.F.);
#4073=ADVANCED_FACE('',(#758),#3908,.F.);
#4074=ADVANCED_FACE('',(#759),#3909,.F.);
#4075=ADVANCED_FACE('',(#760),#3910,.F.);
#4076=ADVANCED_FACE('',(#761),#3911,.T.);
#4077=ADVANCED_FACE('',(#762),#261,.T.);
#4078=ADVANCED_FACE('',(#763),#614,.T.);
#4079=ADVANCED_FACE('',(#764),#262,.T.);
#4080=ADVANCED_FACE('',(#765,#380),#3912,.T.);
#4081=ADVANCED_FACE('',(#766),#263,.T.);
#4082=ADVANCED_FACE('',(#767),#615,.T.);
#4203=CLOSED_SHELL('',(#4067,#4068,#4069,#4070,#4071,#4072,#4073,#4074));
#4204=CLOSED_SHELL('',(#4075,#4076,#4077,#4078,#4079,#4080,#4081,#4082));
#4573=AXIS2_PLACEMENT_3D('',#6763,#5427,#5428);
#4574=AXIS2_PLACEMENT_3D('',#6764,#5429,#5430);
#4575=AXIS2_PLACEMENT_3D('',#6773,#5435,#5436);
#4576=AXIS2_PLACEMENT_3D('',#6779,#5440,#5441);
#4577=AXIS2_PLACEMENT_3D('',#6785,#5445,#5446);
#4578=AXIS2_PLACEMENT_3D('',#6791,#5450,#5451);
#4579=AXIS2_PLACEMENT_3D('',#6797,#5455,#5456);
#4580=AXIS2_PLACEMENT_3D('',#6800,#5459,#5460);
#4581=AXIS2_PLACEMENT_3D('',#6801,#5461,#5462);
#4582=AXIS2_PLACEMENT_3D('',#6802,#5463,#5464);
#4583=AXIS2_PLACEMENT_3D('',#6804,#5465,#5466);
#4584=AXIS2_PLACEMENT_3D('',#6805,#5467,#5468);
#4585=AXIS2_PLACEMENT_3D('',#6807,#5469,#5470);
#4586=AXIS2_PLACEMENT_3D('',#6808,#5471,#5472);
#4587=AXIS2_PLACEMENT_3D('',#6810,#5473,#5474);
#4588=AXIS2_PLACEMENT_3D('',#6812,#5476,#5477);
#4589=AXIS2_PLACEMENT_3D('',#6814,#5478,#5479);
#4590=AXIS2_PLACEMENT_3D('',#6816,#5481,#5482);
#4591=AXIS2_PLACEMENT_3D('',#6818,#5483,#5484);
#4592=AXIS2_PLACEMENT_3D('',#6820,#5486,#5487);
#4593=AXIS2_PLACEMENT_3D('',#6822,#5488,#5489);
#4594=AXIS2_PLACEMENT_3D('',#6823,#5490,#5491);
#4595=AXIS2_PLACEMENT_3D('',#6825,#5492,#5493);
#4596=AXIS2_PLACEMENT_3D('',#6827,#5495,#5496);
#5427=DIRECTION('axis',(0.,0.,1.));
#5428=DIRECTION('refdir',(1.,0.,0.));
#5429=DIRECTION('center_axis',(0.866025403784439,0.,-0.5));
#5430=DIRECTION('ref_axis',(0.5,0.,0.866025403784439));
#5431=DIRECTION('',(-0.5,0.,-0.866025403784439));
#5432=DIRECTION('',(0.,-1.,0.));
#5433=DIRECTION('',(0.5,0.,0.866025403784439));
#5434=DIRECTION('',(0.,-1.,0.));
#5435=DIRECTION('center_axis',(1.20185167898973E-16,0.,-1.));
#5436=DIRECTION('ref_axis',(1.,0.,1.20185167898973E-16));
#5437=DIRECTION('',(-1.,0.,-1.20185167898973E-16));
#5438=DIRECTION('',(0.,-1.,0.));
#5439=DIRECTION('',(1.,0.,1.20185167898973E-16));
#5440=DIRECTION('center_axis',(-0.866025403784439,0.,-0.5));
#5441=DIRECTION('ref_axis',(0.5,0.,-0.866025403784439));
#5442=DIRECTION('',(-0.5,0.,0.866025403784439));
#5443=DIRECTION('',(0.,-1.,0.));
#5444=DIRECTION('',(0.5,0.,-0.866025403784439));
#5445=DIRECTION('center_axis',(-0.866025403784439,0.,0.5));
#5446=DIRECTION('ref_axis',(-0.5,0.,-0.866025403784439));
#5447=DIRECTION('',(0.5,0.,0.866025403784439));
#5448=DIRECTION('',(0.,-1.,0.));
#5449=DIRECTION('',(-0.5,0.,-0.866025403784439));
#5450=DIRECTION('center_axis',(-2.40370335797945E-16,0.,1.));
#5451=DIRECTION('ref_axis',(-1.,0.,-2.40370335797945E-16));
#5452=DIRECTION('',(1.,0.,2.40370335797945E-16));
#5453=DIRECTION('',(0.,-1.,0.));
#5454=DIRECTION('',(-1.,0.,-2.40370335797945E-16));
#5455=DIRECTION('center_axis',(0.866025403784439,0.,0.5));
#5456=DIRECTION('ref_axis',(-0.5,0.,0.866025403784439));
#5457=DIRECTION('',(0.5,0.,-0.866025403784439));
#5458=DIRECTION('',(-0.5,0.,0.866025403784439));
#5459=DIRECTION('center_axis',(0.,1.,0.));
#5460=DIRECTION('ref_axis',(1.,0.,0.));
#5461=DIRECTION('center_axis',(0.,-1.,0.));
#5462=DIRECTION('ref_axis',(0.,0.,-1.));
#5463=DIRECTION('center_axis',(0.,1.,0.));
#5464=DIRECTION('ref_axis',(1.,0.,0.));
#5465=DIRECTION('center_axis',(0.,1.,0.));
#5466=DIRECTION('ref_axis',(1.,0.,0.));
#5467=DIRECTION('center_axis',(0.,1.,0.));
#5468=DIRECTION('ref_axis',(0.,0.,1.));
#5469=DIRECTION('center_axis',(0.,-1.,0.));
#5470=DIRECTION('ref_axis',(1.,0.,0.));
#5471=DIRECTION('center_axis',(0.,-1.,0.));
#5472=DIRECTION('ref_axis',(1.,0.,0.));
#5473=DIRECTION('center_axis',(0.,-1.,0.));
#5474=DIRECTION('ref_axis',(1.,0.,0.));
#5475=DIRECTION('',(0.707106781186548,0.707106781186547,8.65956056235493E-17));
#5476=DIRECTION('center_axis',(0.,-1.,0.));
#5477=DIRECTION('ref_axis',(1.,0.,0.));
#5478=DIRECTION('center_axis',(0.,-1.,0.));
#5479=DIRECTION('ref_axis',(1.,0.,0.));
#5480=DIRECTION('',(0.,1.,0.));
#5481=DIRECTION('center_axis',(0.,1.,0.));
#5482=DIRECTION('ref_axis',(1.,0.,0.));
#5483=DIRECTION('center_axis',(0.,-1.,0.));
#5484=DIRECTION('ref_axis',(1.,0.,0.));
#5485=DIRECTION('',(-0.707106781186547,0.707106781186548,-8.65956056235493E-17));
#5486=DIRECTION('center_axis',(0.,-1.,0.));
#5487=DIRECTION('ref_axis',(0.,0.,-1.));
#5488=DIRECTION('center_axis',(0.,-1.,0.));
#5489=DIRECTION('ref_axis',(1.,0.,0.));
#5490=DIRECTION('center_axis',(0.,1.,0.));
#5491=DIRECTION('ref_axis',(1.,0.,0.));
#5492=DIRECTION('center_axis',(0.,1.,0.));
#5493=DIRECTION('ref_axis',(1.,0.,0.));
#5494=DIRECTION('',(-0.447213595499958,0.894427190999916,-5.47678698264203E-17));
#5495=DIRECTION('center_axis',(0.,-1.,0.));
#5496=DIRECTION('ref_axis',(1.,0.,0.));
#5497=DIRECTION('',(0.,1.,0.));
#6763=CARTESIAN_POINT('',(0.,0.,0.));
#6764=CARTESIAN_POINT('Origin',(0.115470053837925,-0.5,-0.2));
#6765=CARTESIAN_POINT('',(0.23094010767585,-0.5,0.));
#6766=CARTESIAN_POINT('',(0.115470053837925,-0.5,-0.2));
#6767=CARTESIAN_POINT('',(0.23094010767585,-0.5,0.));
#6768=CARTESIAN_POINT('',(0.115470053837925,-0.8,-0.2));
#6769=CARTESIAN_POINT('',(0.115470053837925,-0.5,-0.2));
#6770=CARTESIAN_POINT('',(0.23094010767585,-0.8,0.));
#6771=CARTESIAN_POINT('',(0.23094010767585,-0.8,0.));
#6772=CARTESIAN_POINT('',(0.23094010767585,-0.5,0.));
#6773=CARTESIAN_POINT('Origin',(-0.115470053837925,-0.5,-0.2));
#6774=CARTESIAN_POINT('',(-0.115470053837925,-0.5,-0.2));
#6775=CARTESIAN_POINT('',(0.115470053837925,-0.5,-0.2));
#6776=CARTESIAN_POINT('',(-0.115470053837925,-0.8,-0.2));
#6777=CARTESIAN_POINT('',(-0.115470053837925,-0.5,-0.2));
#6778=CARTESIAN_POINT('',(0.115470053837925,-0.8,-0.2));
#6779=CARTESIAN_POINT('Origin',(-0.23094010767585,-0.5,-2.77555756156289E-17));
#6780=CARTESIAN_POINT('',(-0.23094010767585,-0.5,-2.82820063659975E-17));
#6781=CARTESIAN_POINT('',(-0.115470053837925,-0.5,-0.2));
#6782=CARTESIAN_POINT('',(-0.23094010767585,-0.8,-2.77555756156289E-17));
#6783=CARTESIAN_POINT('',(-0.23094010767585,-0.5,-2.82820063659975E-17));
#6784=CARTESIAN_POINT('',(-0.115470053837925,-0.8,-0.2));
#6785=CARTESIAN_POINT('Origin',(-0.115470053837925,-0.5,0.2));
#6786=CARTESIAN_POINT('',(-0.115470053837925,-0.5,0.2));
#6787=CARTESIAN_POINT('',(-0.23094010767585,-0.5,-2.82820063659975E-17));
#6788=CARTESIAN_POINT('',(-0.115470053837925,-0.8,0.2));
#6789=CARTESIAN_POINT('',(-0.115470053837925,-0.5,0.2));
#6790=CARTESIAN_POINT('',(-0.23094010767585,-0.8,-2.82820063659975E-17));
#6791=CARTESIAN_POINT('Origin',(0.115470053837925,-0.5,0.2));
#6792=CARTESIAN_POINT('',(0.115470053837925,-0.5,0.2));
#6793=CARTESIAN_POINT('',(-0.115470053837925,-0.5,0.2));
#6794=CARTESIAN_POINT('',(0.115470053837925,-0.8,0.2));
#6795=CARTESIAN_POINT('',(0.115470053837925,-0.5,0.2));
#6796=CARTESIAN_POINT('',(-0.115470053837925,-0.8,0.2));
#6797=CARTESIAN_POINT('Origin',(0.23094010767585,-0.5,0.));
#6798=CARTESIAN_POINT('',(0.115470053837925,-0.5,0.2));
#6799=CARTESIAN_POINT('',(0.115470053837925,-0.8,0.2));
#6800=CARTESIAN_POINT('Origin',(0.,-0.5,0.));
#6801=CARTESIAN_POINT('Origin',(0.,-0.8,0.));
#6802=CARTESIAN_POINT('Origin',(0.,-1.4,0.));
#6803=CARTESIAN_POINT('',(-0.24505,-1.4,3.00099698131059E-17));
#6804=CARTESIAN_POINT('Origin',(0.,-1.4,0.));
#6805=CARTESIAN_POINT('Origin',(0.375,0.5,0.));
#6806=CARTESIAN_POINT('',(-0.375,0.5,-4.59242549680257E-17));
#6807=CARTESIAN_POINT('Origin',(0.,0.5,0.));
#6808=CARTESIAN_POINT('Origin',(0.,0.475,0.));
#6809=CARTESIAN_POINT('',(-0.425,0.45,-5.20474889637625E-17));
#6810=CARTESIAN_POINT('Origin',(0.,0.45,0.));
#6811=CARTESIAN_POINT('',(-0.4,0.475,-4.89858719658941E-17));
#6812=CARTESIAN_POINT('Origin',(0.,0.24,0.));
#6813=CARTESIAN_POINT('',(-0.425,0.0299999999999998,-5.20474889637625E-17));
#6814=CARTESIAN_POINT('Origin',(0.,0.0299999999999998,0.));
#6815=CARTESIAN_POINT('',(-0.425,0.24,-5.20474889637625E-17));
#6816=CARTESIAN_POINT('Origin',(0.,0.0150000000000001,0.));
#6817=CARTESIAN_POINT('',(-0.395,4.85722573273506E-17,-4.83735485663204E-17));
#6818=CARTESIAN_POINT('Origin',(0.,0.,0.));
#6819=CARTESIAN_POINT('',(-0.41,0.0150000000000001,-5.02105187650415E-17));
#6820=CARTESIAN_POINT('Origin',(0.27,0.,0.));
#6821=CARTESIAN_POINT('',(-0.27,0.,-3.30654635769785E-17));
#6822=CARTESIAN_POINT('Origin',(0.,0.,0.));
#6823=CARTESIAN_POINT('Origin',(0.,-0.02,0.));
#6824=CARTESIAN_POINT('',(-0.24505,-0.0498999999999999,3.00099698131059E-17));
#6825=CARTESIAN_POINT('Origin',(0.,-0.0498999999999999,0.));
#6826=CARTESIAN_POINT('',(-0.26,-0.02,-3.18408167778312E-17));
#6827=CARTESIAN_POINT('Origin',(0.,-0.995,0.));
#6828=CARTESIAN_POINT('',(-0.24505,-0.995,-3.00099698131059E-17));
#7766=UNCERTAINTY_MEASURE_WITH_UNIT(LENGTH_MEASURE(0.001),#7807,
'DISTANCE_ACCURACY_VALUE',
'Maximum model space distance between geometric entities at asserted c
onnectivities');
#7782=UNCERTAINTY_MEASURE_WITH_UNIT(LENGTH_MEASURE(0.001),#7807,
'DISTANCE_ACCURACY_VALUE',
'Maximum model space distance between geometric entities at asserted c
onnectivities');
#7790=(
GEOMETRIC_REPRESENTATION_CONTEXT(3)
GLOBAL_UNCERTAINTY_ASSIGNED_CONTEXT((#7766))
GLOBAL_UNIT_ASSIGNED_CONTEXT((#7807,#7809,#7810))
REPRESENTATION_CONTEXT('','3D')
);
#7806=(
GEOMETRIC_REPRESENTATION_CONTEXT(3)
GLOBAL_UNCERTAINTY_ASSIGNED_CONTEXT((#7782))
GLOBAL_UNIT_ASSIGNED_CONTEXT((#7807,#7809,#7810))
REPRESENTATION_CONTEXT('','3D')
);
#7807=(
LENGTH_UNIT()
NAMED_UNIT(*)
SI_UNIT(.CENTI.,.METRE.)
);
#7809=(
NAMED_UNIT(*)
PLANE_ANGLE_UNIT()
SI_UNIT($,.RADIAN.)
);
#7810=(
NAMED_UNIT(*)
SI_UNIT($,.STERADIAN.)
SOLID_ANGLE_UNIT()
);
#7818=SHAPE_DEFINITION_REPRESENTATION(#7841,#7917);
#7841=PRODUCT_DEFINITION_SHAPE('',$,#7941);
#7917=SHAPE_REPRESENTATION('',(#4573),#7790);
#7933=PRODUCT_DEFINITION_CONTEXT('part definition',#8004,'design');
#7941=PRODUCT_DEFINITION('M5x14 Cap Screw','M5x14 Cap Screw',#7964,#7933);
#7964=PRODUCT_DEFINITION_FORMATION('',$,#8013);
#8004=APPLICATION_CONTEXT(
'Core Data for Automotive Mechanical Design Process');
#8005=PRODUCT_CONTEXT('part definition',#8004,'mechanical');
#8013=PRODUCT('M5x14 Cap Screw','M5x14 Cap Screw','M5x14 Cap Screw',(#8005));
#8092=COLOUR_RGB('Black',0.12,0.14,0.17);
#8093=FILL_AREA_STYLE_COLOUR('',#8092);
#8094=FILL_AREA_STYLE('',(#8093));
#8095=SURFACE_STYLE_FILL_AREA(#8094);
#8096=SURFACE_SIDE_STYLE('',(#8095));
#8097=SURFACE_STYLE_USAGE(.BOTH.,#8096);
#8098=PRESENTATION_STYLE_ASSIGNMENT((#8097));
ENDSEC;
END-ISO-10303-21;
